ISO-10303-21;
HEADER;
/* Generated by software containing ST-Developer
 * from STEP Tools, Inc. (www.steptools.com) 
 */

FILE_DESCRIPTION(
/* description */ (
'Independent manual bench leaf bending machine,200mm work width. Fabri
cated welded frame and folding leaf, repeated bushed and fully retaine
d hinge hardware, two handles with bonded grips, beveled clamping beam
 and modeledM12 clamp screws.2mm omitted-workpiece assembly reference 
gap, not a capacity claim. Native135deg hinge travel. Weld sizing, pro
duction fits, material condition, bending capacity, strength and life 
unassigned.'),
/* implementation_level */ '2;1');

FILE_NAME(
/* name */ 'Hinge thrust washer.step',
/* time_stamp */ '2026-11-14T09:11:34-08:00',
/* author */ (''),
/* organization */ (''),
/* preprocessor_version */ 'ST-DEVELOPER v20.2',
/* originating_system */ 'Autodesk Translation Framework v15.17.0.0',
/* authorisation */ '');

FILE_SCHEMA (('AUTOMOTIVE_DESIGN { 1 0 10303 214 3 1 1 }'));
ENDSEC;

DATA;
#10=MECHANICAL_DESIGN_GEOMETRIC_PRESENTATION_REPRESENTATION('',(#462),#37701);
#426=SHAPE_REPRESENTATION_RELATIONSHIP('SRR','None',#37795,#444);
#444=ADVANCED_BREP_SHAPE_REPRESENTATION('',(#480),#37699);
#462=STYLED_ITEM('',(#37880),#480);
#480=MANIFOLD_SOLID_BREP('Body1',#4160);
#514=FACE_BOUND('',#1051,.T.);
#515=FACE_BOUND('',#1053,.T.);
#596=PLANE('',#4660);
#597=PLANE('',#4661);
#804=FACE_OUTER_BOUND('',#1048,.T.);
#805=FACE_OUTER_BOUND('',#1049,.T.);
#806=FACE_OUTER_BOUND('',#1050,.T.);
#807=FACE_OUTER_BOUND('',#1052,.T.);
#1048=EDGE_LOOP('',(#3775,#3776,#3777,#3778));
#1049=EDGE_LOOP('',(#3779,#3780,#3781,#3782));
#1050=EDGE_LOOP('',(#3783));
#1051=EDGE_LOOP('',(#3784));
#1052=EDGE_LOOP('',(#3785));
#1053=EDGE_LOOP('',(#3786));
#1299=LINE('',#37591,#1548);
#1300=LINE('',#37597,#1549);
#1548=VECTOR('',#5536,6.);
#1549=VECTOR('',#5543,11.);
#1629=CIRCLE('',#4655,6.);
#1630=CIRCLE('',#4656,6.);
#1631=CIRCLE('',#4658,11.);
#1632=CIRCLE('',#4659,11.);
#2041=VERTEX_POINT('',#37588);
#2042=VERTEX_POINT('',#37590);
#2043=VERTEX_POINT('',#37594);
#2044=VERTEX_POINT('',#37596);
#2621=EDGE_CURVE('',#2041,#2041,#1629,.T.);
#2622=EDGE_CURVE('',#2041,#2042,#1299,.T.);
#2623=EDGE_CURVE('',#2042,#2042,#1630,.T.);
#2624=EDGE_CURVE('',#2043,#2043,#1631,.T.);
#2625=EDGE_CURVE('',#2043,#2044,#1300,.T.);
#2626=EDGE_CURVE('',#2044,#2044,#1632,.T.);
#3775=ORIENTED_EDGE('',*,*,#2621,.T.);
#3776=ORIENTED_EDGE('',*,*,#2622,.T.);
#3777=ORIENTED_EDGE('',*,*,#2623,.F.);
#3778=ORIENTED_EDGE('',*,*,#2622,.F.);
#3779=ORIENTED_EDGE('',*,*,#2624,.F.);
#3780=ORIENTED_EDGE('',*,*,#2625,.T.);
#3781=ORIENTED_EDGE('',*,*,#2626,.T.);
#3782=ORIENTED_EDGE('',*,*,#2625,.F.);
#3783=ORIENTED_EDGE('',*,*,#2624,.T.);
#3784=ORIENTED_EDGE('',*,*,#2623,.T.);
#3785=ORIENTED_EDGE('',*,*,#2626,.F.);
#3786=ORIENTED_EDGE('',*,*,#2621,.F.);
#3928=CYLINDRICAL_SURFACE('',#4654,6.);
#3929=CYLINDRICAL_SURFACE('',#4657,11.);
#4134=ADVANCED_FACE('',(#804),#3928,.F.);
#4135=ADVANCED_FACE('',(#805),#3929,.T.);
#4136=ADVANCED_FACE('',(#806,#514),#596,.T.);
#4137=ADVANCED_FACE('',(#807,#515),#597,.F.);
#4160=CLOSED_SHELL('',(#4134,#4135,#4136,#4137));
#4653=AXIS2_PLACEMENT_3D('',#37586,#5530,#5531);
#4654=AXIS2_PLACEMENT_3D('',#37587,#5532,#5533);
#4655=AXIS2_PLACEMENT_3D('',#37589,#5534,#5535);
#4656=AXIS2_PLACEMENT_3D('',#37592,#5537,#5538);
#4657=AXIS2_PLACEMENT_3D('',#37593,#5539,#5540);
#4658=AXIS2_PLACEMENT_3D('',#37595,#5541,#5542);
#4659=AXIS2_PLACEMENT_3D('',#37598,#5544,#5545);
#4660=AXIS2_PLACEMENT_3D('',#37599,#5546,#5547);
#4661=AXIS2_PLACEMENT_3D('',#37600,#5548,#5549);
#5530=DIRECTION('axis',(0.,0.,1.));
#5531=DIRECTION('refdir',(1.,0.,0.));
#5532=DIRECTION('center_axis',(0.,0.,1.));
#5533=DIRECTION('ref_axis',(1.,0.,0.));
#5534=DIRECTION('center_axis',(0.,0.,-1.));
#5535=DIRECTION('ref_axis',(1.,0.,0.));
#5536=DIRECTION('',(0.,0.,1.));
#5537=DIRECTION('center_axis',(0.,0.,-1.));
#5538=DIRECTION('ref_axis',(1.,0.,0.));
#5539=DIRECTION('center_axis',(0.,0.,1.));
#5540=DIRECTION('ref_axis',(1.,0.,0.));
#5541=DIRECTION('center_axis',(0.,0.,1.));
#5542=DIRECTION('ref_axis',(1.,0.,0.));
#5543=DIRECTION('',(0.,0.,-1.));
#5544=DIRECTION('center_axis',(0.,0.,1.));
#5545=DIRECTION('ref_axis',(1.,0.,0.));
#5546=DIRECTION('center_axis',(0.,0.,1.));
#5547=DIRECTION('ref_axis',(1.,0.,0.));
#5548=DIRECTION('center_axis',(0.,0.,1.));
#5549=DIRECTION('ref_axis',(1.,0.,0.));
#37586=CARTESIAN_POINT('',(0.,0.,0.));
#37587=CARTESIAN_POINT('Origin',(0.,0.,0.));
#37588=CARTESIAN_POINT('',(-6.,-7.34788079488412E-16,0.));
#37589=CARTESIAN_POINT('Origin',(0.,0.,0.));
#37590=CARTESIAN_POINT('',(-6.,-7.34788079488412E-16,2.));
#37591=CARTESIAN_POINT('',(-6.,-7.34788079488412E-16,0.));
#37592=CARTESIAN_POINT('Origin',(0.,0.,2.));
#37593=CARTESIAN_POINT('Origin',(0.,0.,0.));
#37594=CARTESIAN_POINT('',(-11.,-1.34711147906209E-15,2.));
#37595=CARTESIAN_POINT('Origin',(0.,0.,2.));
#37596=CARTESIAN_POINT('',(-11.,-1.34711147906209E-15,0.));
#37597=CARTESIAN_POINT('',(-11.,-1.34711147906209E-15,0.));
#37598=CARTESIAN_POINT('Origin',(0.,0.,0.));
#37599=CARTESIAN_POINT('Origin',(0.,0.,2.));
#37600=CARTESIAN_POINT('Origin',(0.,0.,0.));
#37679=UNCERTAINTY_MEASURE_WITH_UNIT(LENGTH_MEASURE(0.01),#37702,
'DISTANCE_ACCURACY_VALUE',
'Maximum model space distance between geometric entities at asserted c
onnectivities');
#37681=UNCERTAINTY_MEASURE_WITH_UNIT(LENGTH_MEASURE(0.01),#37702,
'DISTANCE_ACCURACY_VALUE',
'Maximum model space distance between geometric entities at asserted c
onnectivities');
#37699=(
GEOMETRIC_REPRESENTATION_CONTEXT(3)
GLOBAL_UNCERTAINTY_ASSIGNED_CONTEXT((#37679))
GLOBAL_UNIT_ASSIGNED_CONTEXT((#37702,#37704,#37705))
REPRESENTATION_CONTEXT('','3D')
);
#37701=(
GEOMETRIC_REPRESENTATION_CONTEXT(3)
GLOBAL_UNCERTAINTY_ASSIGNED_CONTEXT((#37681))
GLOBAL_UNIT_ASSIGNED_CONTEXT((#37702,#37704,#37705))
REPRESENTATION_CONTEXT('','3D')
);
#37702=(
LENGTH_UNIT()
NAMED_UNIT(*)
SI_UNIT(.MILLI.,.METRE.)
);
#37704=(
NAMED_UNIT(*)
PLANE_ANGLE_UNIT()
SI_UNIT($,.RADIAN.)
);
#37705=(
NAMED_UNIT(*)
SI_UNIT($,.STERADIAN.)
SOLID_ANGLE_UNIT()
);
#37723=SHAPE_DEFINITION_REPRESENTATION(#37742,#37795);
#37742=PRODUCT_DEFINITION_SHAPE('',$,#37815);
#37795=SHAPE_REPRESENTATION('',(#4653),#37699);
#37797=PRODUCT_DEFINITION_CONTEXT('part definition',#37856,'design');
#37815=PRODUCT_DEFINITION('Hinge thrust washer','Hinge thrust washer',#37834,
#37797);
#37834=PRODUCT_DEFINITION_FORMATION('',$,#37875);
#37856=APPLICATION_CONTEXT(
'Core Data for Automotive Mechanical Design Process');
#37857=PRODUCT_CONTEXT('part definition',#37856,'mechanical');
#37875=PRODUCT('Hinge thrust washer','Hinge thrust washer',$,(#37857));
#37880=PRESENTATION_STYLE_ASSIGNMENT((#37888));
#37888=SURFACE_STYLE_USAGE(.BOTH.,#37896);
#37896=SURFACE_SIDE_STYLE('',(#37904));
#37904=SURFACE_STYLE_FILL_AREA(#37912);
#37912=FILL_AREA_STYLE('Opaque(185,192,202)',(#37920));
#37920=FILL_AREA_STYLE_COLOUR('Opaque(185,192,202)',#37928);
#37928=COLOUR_RGB('Opaque(185,192,202)',0.725490196078431,0.752941176470588,
0.792156862745098);
ENDSEC;
END-ISO-10303-21;
